ISO-10303-21;
HEADER;
FILE_DESCRIPTION (('STEP AP203'),
    '1' );
FILE_NAME ('Nut_Predeterminado.step',
    '2026-10-08T11:28:20',
    ( '' ),
    ( '' ),
    'SwSTEP 2.0',
    'SolidWorks 2024',
    '' );
FILE_SCHEMA (( 'AUTOMOTIVE_DESIGN' ));
ENDSEC;

DATA;
#49=DIRECTION ( 'NONE',  ( -0.002879925520664897674, 0.000000000000000000, -0.9999958530058988826 ) ) ;
#111=ORIENTED_EDGE ( 'NONE', *, *, #10885, .F. ) ;
#142=CARTESIAN_POINT ( 'NONE',  ( 0.000000000000000000, 5.000000000000000000, -3.500000000000000000 ) ) ;
#276=AXIS2_PLACEMENT_3D ( 'NONE', #7500, #13311, #2716 ) ;
#281=FACE_OUTER_BOUND ( 'NONE', #1053, .T. ) ;
#352=FACE_OUTER_BOUND ( 'NONE', #11436, .T. ) ;
#369=ORIENTED_EDGE ( 'NONE', *, *, #451, .F. ) ;
#378=DIRECTION ( 'NONE',  ( -0.002879925520667554837, 0.000000000000000000, -0.9999958530058988826 ) ) ;
#390=CYLINDRICAL_SURFACE ( 'NONE', #5044, 3.500000000000000000 ) ;
#406=CARTESIAN_POINT ( 'NONE',  ( 4.492499072540838689, 0.000000000000000000, -2.611025101989581820 ) ) ;
#451=EDGE_CURVE ( 'NONE', #887, #14484, #14806, .T. ) ;
#457=DIRECTION ( 'NONE',  ( -0.000000000000000000, -1.000000000000000000, -0.000000000000000000 ) ) ;
#474=CARTESIAN_POINT ( 'NONE',  ( -4.507463604512252253, 5.000000000000000000, -2.585105772303598393 ) ) ;
#511=CARTESIAN_POINT ( 'NONE',  ( 0.000000000000000000, 5.000000000000000000, -3.500000000000000000 ) ) ;
#626=LINE ( 'NONE', #13538, #7670 ) ;
#637=ORIENTED_EDGE ( 'NONE', *, *, #12424, .T. ) ;
#698=VERTEX_POINT ( 'NONE', #7415 ) ;
#716=DIRECTION ( 'NONE',  ( 0.8674617751425296452, 0.000000000000000000, 0.4975038378410473472 ) ) ;
#750=VERTEX_POINT ( 'NONE', #4948 ) ;
#801=EDGE_CURVE ( 'NONE', #750, #698, #14396, .T. ) ;
#830=DIRECTION ( 'NONE',  ( 0.8645818496218652394, 0.000000000000000000, -0.5024920151648527566 ) ) ;
#857=CARTESIAN_POINT ( 'NONE',  ( 0.000000000000000000, 0.000000000000000000, -3.500000000000000000 ) ) ;
#880=DIRECTION ( 'NONE',  ( -0.8674617751425297563, 0.000000000000000000, -0.4975038378410474027 ) ) ;
#887=VERTEX_POINT ( 'NONE', #474 ) ;
#1027=VERTEX_POINT ( 'NONE', #857 ) ;
#1048=ORIENTED_EDGE ( 'NONE', *, *, #1468, .F. ) ;
#1053=EDGE_LOOP ( 'NONE', ( #12778, #8600, #2407, #11031 ) ) ;
#1067=VECTOR ( 'NONE', #3211, 1000.000000000000000 ) ;
#1137=SHAPE_DEFINITION_REPRESENTATION ( #3882, #9812 ) ;
#1158=PLANE ( 'NONE',  #8481 ) ;
#1180=ORIENTED_EDGE ( 'NONE', *, *, #7997, .T. ) ;
#1255=VERTEX_POINT ( 'NONE', #8176 ) ;
#1380=DIRECTION ( 'NONE',  ( -0.000000000000000000, -1.000000000000000000, -0.000000000000000000 ) ) ;
#1416=CLOSED_SHELL ( 'NONE', ( #7233, #7342, #7908, #10328, #15168, #10833, #14727, #3095, #12647, #10715 ) ) ;
#1437=CARTESIAN_POINT ( 'NONE',  ( 4.507463604512255806, 0.000000000000000000, 2.585105772303601945 ) ) ;
#1468=EDGE_CURVE ( 'NONE', #15191, #1027, #7393, .T. ) ;
#1470=CARTESIAN_POINT ( 'NONE',  ( 4.507463604512255806, 5.000000000000000000, 2.585105772303601945 ) ) ;
#1475=EDGE_LOOP ( 'NONE', ( #14338, #13003, #3123, #7578 ) ) ;
#1520=VECTOR ( 'NONE', #6716, 999.9999999999998863 ) ;
#1584=EDGE_CURVE ( 'NONE', #7183, #12677, #2616, .T. ) ;
#1630=LINE ( 'NONE', #5190, #11951 ) ;
#1724=AXIS2_PLACEMENT_3D ( 'NONE', #2035, #11460, #880 ) ;
#1728=EDGE_CURVE ( 'NONE', #11635, #4915, #9804, .T. ) ;
#1757=AXIS2_PLACEMENT_3D ( 'NONE', #9874, #2688, #378 ) ;
#1763=DIRECTION ( 'NONE',  ( -0.000000000000000000, -1.000000000000000000, -0.000000000000000000 ) ) ;
#1768=( GEOMETRIC_REPRESENTATION_CONTEXT ( 3 ) GLOBAL_UNCERTAINTY_ASSIGNED_CONTEXT ( ( #14226 ) ) GLOBAL_UNIT_ASSIGNED_CONTEXT ( ( #5521, #4369, #6899 ) ) REPRESENTATION_CONTEXT ( 'NONE', 'WORKASPACE' ) );
#1811=ORIENTED_EDGE ( 'NONE', *, *, #451, .T. ) ;
#1813=LINE ( 'NONE', #6600, #9229 ) ;
#1889=ORIENTED_EDGE ( 'NONE', *, *, #1728, .F. ) ;
#1911=CARTESIAN_POINT ( 'NONE',  ( 4.507463604512255806, 5.000000000000000000, 2.585105772303601945 ) ) ;
#1951=DIRECTION ( 'NONE',  ( -0.8674617751425300893, 0.000000000000000000, -0.4975038378410468476 ) ) ;
#2005=LINE ( 'NONE', #9969, #1520 ) ;
#2035=CARTESIAN_POINT ( 'NONE',  ( -4.492499072540820926, 5.000000000000000000, 2.611025101989610686 ) ) ;
#2043=EDGE_LOOP ( 'NONE', ( #11614, #9520, #3342, #7597 ) ) ;
#2156=EDGE_CURVE ( 'NONE', #1027, #7762, #11853, .T. ) ;
#2183=FACE_OUTER_BOUND ( 'NONE', #13177, .T. ) ;
#2199=CARTESIAN_POINT ( 'NONE',  ( -0.01496453197141594735, 0.000000000000000000, -5.196130874293185542 ) ) ;
#2296=VECTOR ( 'NONE', #2879, 999.9999999999998863 ) ;
#2407=ORIENTED_EDGE ( 'NONE', *, *, #2737, .F. ) ;
#2508=EDGE_LOOP ( 'NONE', ( #10659, #8618, #8000, #4039, #6161, #4005 ) ) ;
#2522=LINE ( 'NONE', #6063, #11110 ) ;
#2590=CARTESIAN_POINT ( 'NONE',  ( 0.000000000000000000, 5.000000000000000000, 0.000000000000000000 ) ) ;
#2616=LINE ( 'NONE', #7318, #13359 ) ;
#2688=DIRECTION ( 'NONE',  ( 0.9999958530058989936, 0.000000000000000000, -0.002879925520667555271 ) ) ;
#2716=DIRECTION ( 'NONE',  ( 0.000000000000000000, 0.000000000000000000, 1.000000000000000000 ) ) ;
#2737=EDGE_CURVE ( 'NONE', #698, #7183, #9774, .T. ) ;
#2770=FACE_OUTER_BOUND ( 'NONE', #5899, .T. ) ;
#2841=DIRECTION ( 'NONE',  ( 0.000000000000000000, 1.000000000000000000, 0.000000000000000000 ) ) ;
#2879=DIRECTION ( 'NONE',  ( -0.8645818496218652394, 0.000000000000000000, 0.5024920151648527566 ) ) ;
#2887=CARTESIAN_POINT ( 'NONE',  ( -4.492499072540820926, 0.000000000000000000, 2.611025101989610686 ) ) ;
#2917=EDGE_LOOP ( 'NONE', ( #3608, #10118 ) ) ;
#2957=DIRECTION ( 'NONE',  ( 0.000000000000000000, 1.000000000000000000, 0.000000000000000000 ) ) ;
#2997=VECTOR ( 'NONE', #716, 1000.000000000000227 ) ;
#3016=DIRECTION ( 'NONE',  ( 0.8645818496218656835, 0.000000000000000000, -0.5024920151648518685 ) ) ;
#3095=ADVANCED_FACE ( 'NONE', ( #2183 ), #9139, .F. ) ;
#3123=ORIENTED_EDGE ( 'NONE', *, *, #801, .F. ) ;
#3143=MECHANICAL_CONTEXT ( 'NONE', #6610, 'mechanical' ) ;
#3211=DIRECTION ( 'NONE',  ( -0.000000000000000000, -1.000000000000000000, -0.000000000000000000 ) ) ;
#3248=DIRECTION ( 'NONE',  ( 0.002879925520664897674, 0.000000000000000000, 0.9999958530058988826 ) ) ;
#3342=ORIENTED_EDGE ( 'NONE', *, *, #7997, .F. ) ;
#3360=ORIENTED_EDGE ( 'NONE', *, *, #12050, .T. ) ;
#3563=CARTESIAN_POINT ( 'NONE',  ( 0.01496453197139708223, 0.000000000000000000, 5.196130874293197088 ) ) ;
#3570=CIRCLE ( 'NONE', #13702, 3.500000000000000000 ) ;
#3593=FACE_OUTER_BOUND ( 'NONE', #6576, .T. ) ;
#3608=ORIENTED_EDGE ( 'NONE', *, *, #12050, .F. ) ;
#3678=ORIENTED_EDGE ( 'NONE', *, *, #13822, .T. ) ;
#3747=CYLINDRICAL_SURFACE ( 'NONE', #3793, 3.500000000000000000 ) ;
#3793=AXIS2_PLACEMENT_3D ( 'NONE', #2590, #9777, #14509 ) ;
#3836=EDGE_CURVE ( 'NONE', #1255, #5136, #10628, .T. ) ;
#3882=PRODUCT_DEFINITION_SHAPE ( 'NONE', 'NONE',  #8872 ) ;
#3922=EDGE_CURVE ( 'NONE', #4505, #4915, #2522, .T. ) ;
#3928=CARTESIAN_POINT ( 'NONE',  ( 4.286263797015736595E-16, 5.000000000000000000, 3.500000000000000000 ) ) ;
#3977=VECTOR ( 'NONE', #457, 1000.000000000000000 ) ;
#4005=ORIENTED_EDGE ( 'NONE', *, *, #12260, .F. ) ;
#4022=FACE_OUTER_BOUND ( 'NONE', #2043, .T. ) ;
#4039=ORIENTED_EDGE ( 'NONE', *, *, #13822, .F. ) ;
#4065=CARTESIAN_POINT ( 'NONE',  ( 4.492499072540838689, 5.000000000000000000, -2.611025101989581820 ) ) ;
#4108=CARTESIAN_POINT ( 'NONE',  ( -4.492499072540820926, 5.000000000000000000, 2.611025101989610686 ) ) ;
#4132=CARTESIAN_POINT ( 'NONE',  ( -4.507463604512252253, 5.000000000000000000, -2.585105772303598393 ) ) ;
#4140=DIRECTION ( 'NONE',  ( -0.000000000000000000, -1.000000000000000000, -0.000000000000000000 ) ) ;
#4168=ORIENTED_EDGE ( 'NONE', *, *, #14458, .F. ) ;
#4280=DIRECTION ( 'NONE',  ( 0.000000000000000000, 0.000000000000000000, 1.000000000000000000 ) ) ;
#4369=( NAMED_UNIT ( * ) PLANE_ANGLE_UNIT ( ) SI_UNIT ( $, .RADIAN. ) );
#4376=ORIENTED_EDGE ( 'NONE', *, *, #14699, .F. ) ;
#4441=VECTOR ( 'NONE', #49, 1000.000000000000227 ) ;
#4505=VERTEX_POINT ( 'NONE', #2887 ) ;
#4512=EDGE_CURVE ( 'NONE', #7762, #1027, #9137, .T. ) ;
#4687=EDGE_LOOP ( 'NONE', ( #7061, #10452 ) ) ;
#4776=AXIS2_PLACEMENT_3D ( 'NONE', #13897, #13459, #830 ) ;
#4812=CARTESIAN_POINT ( 'NONE',  ( 4.286263797015736595E-16, 5.000000000000000000, 3.500000000000000000 ) ) ;
#4915=VERTEX_POINT ( 'NONE', #3563 ) ;
#4948=CARTESIAN_POINT ( 'NONE',  ( 4.507463604512255806, 5.000000000000000000, 2.585105772303601945 ) ) ;
#4992=PRODUCT ( 'Nut_Predeterminado', 'Nut_Predeterminado', '', ( #3143 ) ) ;
#5008=PLANE ( 'NONE',  #1757 ) ;
#5034=DIRECTION ( 'NONE',  ( -0.000000000000000000, -1.000000000000000000, -0.000000000000000000 ) ) ;
#5044=AXIS2_PLACEMENT_3D ( 'NONE', #10178, #8007, #10323 ) ;
#5136=VERTEX_POINT ( 'NONE', #8157 ) ;
#5190=CARTESIAN_POINT ( 'NONE',  ( -4.492499072540820926, 5.000000000000000000, 2.611025101989610686 ) ) ;
#5349=EDGE_CURVE ( 'NONE', #4915, #1255, #626, .T. ) ;
#5357=LINE ( 'NONE', #12618, #12708 ) ;
#5403=ORIENTED_EDGE ( 'NONE', *, *, #14458, .T. ) ;
#5521=( LENGTH_UNIT ( ) NAMED_UNIT ( * ) SI_UNIT ( .MILLI., .METRE. ) );
#5585=FACE_BOUND ( 'NONE', #2917, .T. ) ;
#5610=APPLICATION_CONTEXT ( 'configuration controlled 3d designs of mechanical parts and assemblies' ) ;
#5740=AXIS2_PLACEMENT_3D ( 'NONE', #12393, #14967, #6525 ) ;
#5822=DIRECTION ( 'NONE',  ( -0.8645818496218656835, 0.000000000000000000, 0.5024920151648518685 ) ) ;
#5840=LINE ( 'NONE', #9402, #10240 ) ;
#5899=EDGE_LOOP ( 'NONE', ( #3678, #15281, #369, #9461 ) ) ;
#6063=CARTESIAN_POINT ( 'NONE',  ( -4.492499072540820926, 0.000000000000000000, 2.611025101989610686 ) ) ;
#6161=ORIENTED_EDGE ( 'NONE', *, *, #11493, .F. ) ;
#6326=ORIENTED_EDGE ( 'NONE', *, *, #13958, .F. ) ;
#6333=PLANE ( 'NONE',  #4776 ) ;
#6413=VECTOR ( 'NONE', #9847, 1000.000000000000000 ) ;
#6422=PLANE ( 'NONE',  #7992 ) ;
#6523=ORIENTED_EDGE ( 'NONE', *, *, #2156, .F. ) ;
#6525=DIRECTION ( 'NONE',  ( 0.000000000000000000, -0.000000000000000000, 1.000000000000000000 ) ) ;
#6544=CARTESIAN_POINT ( 'NONE',  ( 4.492499072540838689, 5.000000000000000000, -2.611025101989581820 ) ) ;
#6576=EDGE_LOOP ( 'NONE', ( #13071, #111, #4168, #8513 ) ) ;
#6585=LINE ( 'NONE', #10139, #2997 ) ;
#6600=CARTESIAN_POINT ( 'NONE',  ( -4.507463604512252253, 5.000000000000000000, -2.585105772303598393 ) ) ;
#6610=APPLICATION_CONTEXT ( 'configuration controlled 3d designs of mechanical parts and assemblies' ) ;
#6716=DIRECTION ( 'NONE',  ( 0.8645818496218656835, 0.000000000000000000, -0.5024920151648518685 ) ) ;
#6731=DIRECTION ( 'NONE',  ( -0.9999958530058989936, 0.000000000000000000, 0.002879925520664898108 ) ) ;
#6899=( NAMED_UNIT ( * ) SI_UNIT ( $, .STERADIAN. ) SOLID_ANGLE_UNIT ( ) );
#7061=ORIENTED_EDGE ( 'NONE', *, *, #2156, .T. ) ;
#7183=VERTEX_POINT ( 'NONE', #14663 ) ;
#7205=CARTESIAN_POINT ( 'NONE',  ( 0.01496453197139708223, 5.000000000000000000, 5.196130874293197088 ) ) ;
#7233=ADVANCED_FACE ( 'NONE', ( #352 ), #3747, .F. ) ;
#7318=CARTESIAN_POINT ( 'NONE',  ( -0.01496453197141594735, 5.000000000000000000, -5.196130874293185542 ) ) ;
#7320=EDGE_CURVE ( 'NONE', #887, #10395, #1813, .T. ) ;
#7342=ADVANCED_FACE ( 'NONE', ( #12701, #5585 ), #11388, .T. ) ;
#7393=LINE ( 'NONE', #142, #7407 ) ;
#7407=VECTOR ( 'NONE', #1380, 1000.000000000000000 ) ;
#7414=ADVANCED_BREP_SHAPE_REPRESENTATION ( '', ( #12143, #9419 ), #1768 ) ;
#7415=CARTESIAN_POINT ( 'NONE',  ( 4.492499072540838689, 5.000000000000000000, -2.611025101989581820 ) ) ;
#7463=CARTESIAN_POINT ( 'NONE',  ( 0.000000000000000000, 5.000000000000000000, 0.000000000000000000 ) ) ;
#7500=CARTESIAN_POINT ( 'NONE',  ( 0.000000000000000000, 0.000000000000000000, 0.000000000000000000 ) ) ;
#7578=ORIENTED_EDGE ( 'NONE', *, *, #10885, .T. ) ;
#7597=ORIENTED_EDGE ( 'NONE', *, *, #1584, .T. ) ;
#7670=VECTOR ( 'NONE', #3016, 999.9999999999998863 ) ;
#7685=AXIS2_PLACEMENT_3D ( 'NONE', #7463, #2841, #13435 ) ;
#7762=VERTEX_POINT ( 'NONE', #13846 ) ;
#7778=DIRECTION ( 'NONE',  ( -0.000000000000000000, -1.000000000000000000, -0.000000000000000000 ) ) ;
#7908=ADVANCED_FACE ( 'NONE', ( #10990, #11141 ), #6422, .F. ) ;
#7990=VECTOR ( 'NONE', #7778, 1000.000000000000000 ) ;
#7992=AXIS2_PLACEMENT_3D ( 'NONE', #406, #9830, #14562 ) ;
#7997=EDGE_CURVE ( 'NONE', #7183, #887, #9909, .T. ) ;
#8000=ORIENTED_EDGE ( 'NONE', *, *, #3922, .F. ) ;
#8007=DIRECTION ( 'NONE',  ( -0.000000000000000000, -1.000000000000000000, -0.000000000000000000 ) ) ;
#8022=ORIENTED_EDGE ( 'NONE', *, *, #13958, .T. ) ;
#8062=VECTOR ( 'NONE', #11154, 1000.000000000000114 ) ;
#8157=CARTESIAN_POINT ( 'NONE',  ( 4.492499072540838689, 0.000000000000000000, -2.611025101989581820 ) ) ;
#8176=CARTESIAN_POINT ( 'NONE',  ( 4.507463604512255806, 0.000000000000000000, 2.585105772303601945 ) ) ;
#8270=DIRECTION ( 'NONE',  ( -0.002879925520664897674, 0.000000000000000000, -0.9999958530058988826 ) ) ;
#8294=PLANE ( 'NONE',  #9997 ) ;
#8381=PLANE ( 'NONE',  #12883 ) ;
#8459=DIRECTION ( 'NONE',  ( 0.8674617751425296452, 0.000000000000000000, 0.4975038378410473472 ) ) ;
#8461=CARTESIAN_POINT ( 'NONE',  ( 4.492499072540838689, 5.000000000000000000, -2.611025101989581820 ) ) ;
#8481=AXIS2_PLACEMENT_3D ( 'NONE', #14072, #6731, #3248 ) ;
#8513=ORIENTED_EDGE ( 'NONE', *, *, #1728, .T. ) ;
#8600=ORIENTED_EDGE ( 'NONE', *, *, #1584, .F. ) ;
#8618=ORIENTED_EDGE ( 'NONE', *, *, #5349, .F. ) ;
#8674=CIRCLE ( 'NONE', #7685, 3.500000000000000000 ) ;
#8701=DIRECTION ( 'NONE',  ( 0.002879925520667554837, 0.000000000000000000, 0.9999958530058988826 ) ) ;
#8872=PRODUCT_DEFINITION ( 'UNKNOWN', '', #11824, #12369 ) ;
#8990=EDGE_LOOP ( 'NONE', ( #4376, #12873, #15285, #10534 ) ) ;
#9009=EDGE_CURVE ( 'NONE', #698, #5136, #13811, .T. ) ;
#9137=CIRCLE ( 'NONE', #13358, 3.500000000000000000 ) ;
#9139=PLANE ( 'NONE',  #1724 ) ;
#9226=DIRECTION ( 'NONE',  ( 0.000000000000000000, 0.000000000000000000, 1.000000000000000000 ) ) ;
#9229=VECTOR ( 'NONE', #4140, 1000.000000000000000 ) ;
#9310=ORIENTED_EDGE ( 'NONE', *, *, #14699, .T. ) ;
#9349=FACE_OUTER_BOUND ( 'NONE', #1475, .T. ) ;
#9402=CARTESIAN_POINT ( 'NONE',  ( -0.01496453197141594735, 0.000000000000000000, -5.196130874293185542 ) ) ;
#9419=AXIS2_PLACEMENT_3D ( 'NONE', #15272, #9226, #12943 ) ;
#9461=ORIENTED_EDGE ( 'NONE', *, *, #7320, .T. ) ;
#9520=ORIENTED_EDGE ( 'NONE', *, *, #7320, .F. ) ;
#9774=LINE ( 'NONE', #4065, #6413 ) ;
#9777=DIRECTION ( 'NONE',  ( -0.000000000000000000, -1.000000000000000000, -0.000000000000000000 ) ) ;
#9804=LINE ( 'NONE', #10964, #3977 ) ;
#9812=SHAPE_REPRESENTATION ( 'Nut_Predeterminado', ( #9419 ), #1768 ) ;
#9830=DIRECTION ( 'NONE',  ( 0.000000000000000000, 1.000000000000000000, 0.000000000000000000 ) ) ;
#9847=DIRECTION ( 'NONE',  ( -0.8674617751425300893, 0.000000000000000000, -0.4975038378410468476 ) ) ;
#9868=VERTEX_POINT ( 'NONE', #4812 ) ;
#9874=CARTESIAN_POINT ( 'NONE',  ( -4.507463604512252253, 5.000000000000000000, -2.585105772303598393 ) ) ;
#9909=LINE ( 'NONE', #14643, #2296 ) ;
#9969=CARTESIAN_POINT ( 'NONE',  ( 0.01496453197139708223, 5.000000000000000000, 5.196130874293197088 ) ) ;
#9997=AXIS2_PLACEMENT_3D ( 'NONE', #7205, #15278, #5822 ) ;
#10118=ORIENTED_EDGE ( 'NONE', *, *, #13703, .F. ) ;
#10139=CARTESIAN_POINT ( 'NONE',  ( -4.492499072540820926, 5.000000000000000000, 2.611025101989610686 ) ) ;
#10178=CARTESIAN_POINT ( 'NONE',  ( 0.000000000000000000, 5.000000000000000000, 0.000000000000000000 ) ) ;
#10240=VECTOR ( 'NONE', #11942, 999.9999999999998863 ) ;
#10323=DIRECTION ( 'NONE',  ( 0.000000000000000000, 0.000000000000000000, -1.000000000000000000 ) ) ;
#10328=ADVANCED_FACE ( 'NONE', ( #9349 ), #1158, .F. ) ;
#10395=VERTEX_POINT ( 'NONE', #13848 ) ;
#10452=ORIENTED_EDGE ( 'NONE', *, *, #4512, .T. ) ;
#10534=ORIENTED_EDGE ( 'NONE', *, *, #4512, .F. ) ;
#10628=LINE ( 'NONE', #1437, #4441 ) ;
#10659=ORIENTED_EDGE ( 'NONE', *, *, #3836, .F. ) ;
#10715=ADVANCED_FACE ( 'NONE', ( #13057 ), #390, .F. ) ;
#10833=ADVANCED_FACE ( 'NONE', ( #4022 ), #6333, .F. ) ;
#10874=LINE ( 'NONE', #3928, #11393 ) ;
#10885=EDGE_CURVE ( 'NONE', #750, #1255, #12205, .T. ) ;
#10888=VECTOR ( 'NONE', #8701, 1000.000000000000114 ) ;
#10945=CARTESIAN_POINT ( 'NONE',  ( -4.507463604512252253, 0.000000000000000000, -2.585105772303598393 ) ) ;
#10964=CARTESIAN_POINT ( 'NONE',  ( 0.01496453197139708223, 5.000000000000000000, 5.196130874293197088 ) ) ;
#10990=FACE_OUTER_BOUND ( 'NONE', #2508, .T. ) ;
#11031=ORIENTED_EDGE ( 'NONE', *, *, #9009, .T. ) ;
#11073=CARTESIAN_POINT ( 'NONE',  ( 0.000000000000000000, 0.000000000000000000, 0.000000000000000000 ) ) ;
#11110=VECTOR ( 'NONE', #8459, 1000.000000000000227 ) ;
#11141=FACE_BOUND ( 'NONE', #4687, .T. ) ;
#11154=DIRECTION ( 'NONE',  ( 0.002879925520667554837, 0.000000000000000000, 0.9999958530058988826 ) ) ;
#11155=CARTESIAN_POINT ( 'NONE',  ( 0.000000000000000000, 5.000000000000000000, 0.000000000000000000 ) ) ;
#11217=EDGE_LOOP ( 'NONE', ( #11842, #13603, #1180, #1811, #8022, #5403 ) ) ;
#11324=VECTOR ( 'NONE', #8270, 1000.000000000000227 ) ;
#11388=PLANE ( 'NONE',  #5740 ) ;
#11393=VECTOR ( 'NONE', #11872, 1000.000000000000000 ) ;
#11436=EDGE_LOOP ( 'NONE', ( #3360, #9310, #6523, #1048 ) ) ;
#11460=DIRECTION ( 'NONE',  ( 0.4975038378410474027, 0.000000000000000000, -0.8674617751425297563 ) ) ;
#11493=EDGE_CURVE ( 'NONE', #12677, #10395, #5840, .T. ) ;
#11614=ORIENTED_EDGE ( 'NONE', *, *, #11493, .T. ) ;
#11635=VERTEX_POINT ( 'NONE', #12019 ) ;
#11824=PRODUCT_DEFINITION_FORMATION_WITH_SPECIFIED_SOURCE ( 'ANY', '', #4992, .NOT_KNOWN. ) ;
#11842=ORIENTED_EDGE ( 'NONE', *, *, #801, .T. ) ;
#11853=CIRCLE ( 'NONE', #276, 3.500000000000000000 ) ;
#11872=DIRECTION ( 'NONE',  ( -0.000000000000000000, -1.000000000000000000, -0.000000000000000000 ) ) ;
#11932=ORIENTED_EDGE ( 'NONE', *, *, #3922, .T. ) ;
#11942=DIRECTION ( 'NONE',  ( -0.8645818496218652394, 0.000000000000000000, 0.5024920151648527566 ) ) ;
#11951=VECTOR ( 'NONE', #5034, 1000.000000000000000 ) ;
#12012=DIRECTION ( 'NONE',  ( 0.8674617751425299783, 0.000000000000000000, 0.4975038378410468476 ) ) ;
#12019=CARTESIAN_POINT ( 'NONE',  ( 0.01496453197139708223, 5.000000000000000000, 5.196130874293197088 ) ) ;
#12050=EDGE_CURVE ( 'NONE', #15191, #9868, #3570, .T. ) ;
#12093=DIRECTION ( 'NONE',  ( -0.4975038378410469031, 0.000000000000000000, 0.8674617751425300893 ) ) ;
#12094=LINE ( 'NONE', #10945, #10888 ) ;
#12143=MANIFOLD_SOLID_BREP ( 'Saliente-Extruir1', #1416 ) ;
#12205=LINE ( 'NONE', #1911, #7990 ) ;
#12260=EDGE_CURVE ( 'NONE', #5136, #12677, #5357, .T. ) ;
#12369=DESIGN_CONTEXT ( 'detailed design', #5610, 'design' ) ;
#12393=CARTESIAN_POINT ( 'NONE',  ( 4.492499072540838689, 5.000000000000000000, -2.611025101989581820 ) ) ;
#12424=EDGE_CURVE ( 'NONE', #14484, #4505, #1630, .T. ) ;
#12618=CARTESIAN_POINT ( 'NONE',  ( 4.492499072540838689, 0.000000000000000000, -2.611025101989581820 ) ) ;
#12647=ADVANCED_FACE ( 'NONE', ( #3593 ), #8294, .F. ) ;
#12677=VERTEX_POINT ( 'NONE', #2199 ) ;
#12701=FACE_OUTER_BOUND ( 'NONE', #11217, .T. ) ;
#12708=VECTOR ( 'NONE', #1951, 1000.000000000000000 ) ;
#12778=ORIENTED_EDGE ( 'NONE', *, *, #12260, .T. ) ;
#12873=ORIENTED_EDGE ( 'NONE', *, *, #13703, .T. ) ;
#12883=AXIS2_PLACEMENT_3D ( 'NONE', #8461, #12093, #12012 ) ;
#12943=DIRECTION ( 'NONE',  ( 1.000000000000000000, 0.000000000000000000, 0.000000000000000000 ) ) ;
#13003=ORIENTED_EDGE ( 'NONE', *, *, #9009, .F. ) ;
#13057=FACE_OUTER_BOUND ( 'NONE', #8990, .T. ) ;
#13071=ORIENTED_EDGE ( 'NONE', *, *, #5349, .T. ) ;
#13177=EDGE_LOOP ( 'NONE', ( #11932, #1889, #6326, #637 ) ) ;
#13311=DIRECTION ( 'NONE',  ( 0.000000000000000000, 1.000000000000000000, 0.000000000000000000 ) ) ;
#13358=AXIS2_PLACEMENT_3D ( 'NONE', #11073, #2957, #14730 ) ;
#13359=VECTOR ( 'NONE', #1763, 1000.000000000000000 ) ;
#13435=DIRECTION ( 'NONE',  ( 0.000000000000000000, 0.000000000000000000, 1.000000000000000000 ) ) ;
#13459=DIRECTION ( 'NONE',  ( 0.5024920151648527566, -0.000000000000000000, 0.8645818496218652394 ) ) ;
#13538=CARTESIAN_POINT ( 'NONE',  ( 0.01496453197139708223, 0.000000000000000000, 5.196130874293197088 ) ) ;
#13603=ORIENTED_EDGE ( 'NONE', *, *, #2737, .T. ) ;
#13702=AXIS2_PLACEMENT_3D ( 'NONE', #11155, #15031, #4280 ) ;
#13703=EDGE_CURVE ( 'NONE', #9868, #15191, #8674, .T. ) ;
#13798=SHAPE_REPRESENTATION_RELATIONSHIP ( 'NONE' , 'NONE' ,  #9812, #7414 ) ;
#13811=LINE ( 'NONE', #6544, #1067 ) ;
#13822=EDGE_CURVE ( 'NONE', #10395, #4505, #12094, .T. ) ;
#13846=CARTESIAN_POINT ( 'NONE',  ( 4.286263797015736595E-16, 0.000000000000000000, 3.500000000000000000 ) ) ;
#13848=CARTESIAN_POINT ( 'NONE',  ( -4.507463604512252253, 0.000000000000000000, -2.585105772303598393 ) ) ;
#13897=CARTESIAN_POINT ( 'NONE',  ( -0.01496453197141594735, 5.000000000000000000, -5.196130874293185542 ) ) ;
#13958=EDGE_CURVE ( 'NONE', #14484, #11635, #6585, .T. ) ;
#14072=CARTESIAN_POINT ( 'NONE',  ( 4.507463604512255806, 5.000000000000000000, 2.585105772303601945 ) ) ;
#14226=UNCERTAINTY_MEASURE_WITH_UNIT (LENGTH_MEASURE( 1.000000000000000082E-05 ), #5521, 'distance_accuracy_value', 'NONE');
#14338=ORIENTED_EDGE ( 'NONE', *, *, #3836, .T. ) ;
#14396=LINE ( 'NONE', #1470, #11324 ) ;
#14458=EDGE_CURVE ( 'NONE', #11635, #750, #2005, .T. ) ;
#14484=VERTEX_POINT ( 'NONE', #4108 ) ;
#14509=DIRECTION ( 'NONE',  ( 0.000000000000000000, 0.000000000000000000, -1.000000000000000000 ) ) ;
#14562=DIRECTION ( 'NONE',  ( 0.000000000000000000, -0.000000000000000000, 1.000000000000000000 ) ) ;
#14643=CARTESIAN_POINT ( 'NONE',  ( -0.01496453197141594735, 5.000000000000000000, -5.196130874293185542 ) ) ;
#14663=CARTESIAN_POINT ( 'NONE',  ( -0.01496453197141594735, 5.000000000000000000, -5.196130874293185542 ) ) ;
#14699=EDGE_CURVE ( 'NONE', #9868, #7762, #10874, .T. ) ;
#14727=ADVANCED_FACE ( 'NONE', ( #2770 ), #5008, .F. ) ;
#14730=DIRECTION ( 'NONE',  ( 0.000000000000000000, 0.000000000000000000, 1.000000000000000000 ) ) ;
#14806=LINE ( 'NONE', #4132, #8062 ) ;
#14967=DIRECTION ( 'NONE',  ( 0.000000000000000000, 1.000000000000000000, 0.000000000000000000 ) ) ;
#15031=DIRECTION ( 'NONE',  ( 0.000000000000000000, 1.000000000000000000, 0.000000000000000000 ) ) ;
#15168=ADVANCED_FACE ( 'NONE', ( #281 ), #8381, .F. ) ;
#15191=VERTEX_POINT ( 'NONE', #511 ) ;
#15272=CARTESIAN_POINT ( 'NONE',  ( 0.000000000000000000, 0.000000000000000000, 0.000000000000000000 ) ) ;
#15278=DIRECTION ( 'NONE',  ( -0.5024920151648518685, 0.000000000000000000, -0.8645818496218656835 ) ) ;
#15281=ORIENTED_EDGE ( 'NONE', *, *, #12424, .F. ) ;
#15285=ORIENTED_EDGE ( 'NONE', *, *, #1468, .T. ) ;
#15360=COLOUR_RGB('Black', 0.09019608, 0.27058824, 0.51372549);
#15361=FILL_AREA_STYLE_COLOUR('',#15360);
#15362=FILL_AREA_STYLE('',(#15361));
#15363=SURFACE_STYLE_FILL_AREA(#15362);
#15364=SURFACE_SIDE_STYLE('',(#15363));
#15365=SURFACE_STYLE_USAGE(.BOTH.,#15364);
#15366=PRESENTATION_STYLE_ASSIGNMENT((#15365));
#15375=STYLED_ITEM('',(#15366),#12143);
#15376=MECHANICAL_DESIGN_GEOMETRIC_PRESENTATION_REPRESENTATION('',(#15375),#1768);
ENDSEC;
END-ISO-10303-21;
